ISO-10303-21;
HEADER;
/* Generated by software containing ST-Developer
 * from STEP Tools, Inc. (www.steptools.com) 
 */

FILE_DESCRIPTION(
/* description */ ('Bearing friction torque test rig'),
/* implementation_level */ '2;1');

FILE_NAME(
/* name */ 'Test bearing collar (1).step',
/* time_stamp */ '2026-10-28T03:24:04-07:00',
/* author */ (''),
/* organization */ (''),
/* preprocessor_version */ 'ST-DEVELOPER v20.2',
/* originating_system */ 'Autodesk Translation Framework v15.17.0.0',
/* authorisation */ '');

FILE_SCHEMA (('AUTOMOTIVE_DESIGN { 1 0 10303 214 3 1 1 }'));
ENDSEC;

DATA;
#10=MECHANICAL_DESIGN_GEOMETRIC_PRESENTATION_REPRESENTATION('',(#590),#14822);
#387=B_SPLINE_CURVE_WITH_KNOTS('',3,(#14457,#14458,#14459,#14460,#14461,
#14462,#14463,#14464,#14465,#14466,#14467,#14468,#14469,#14470),
 .UNSPECIFIED.,.F.,.F.,(4,2,2,2,2,2,4),(0.75600573798702,0.793568827564647,
0.872922520054202,0.952276212543757,1.03162990503331,1.11098359752287,1.14854668710049),
 .UNSPECIFIED.);
#388=B_SPLINE_CURVE_WITH_KNOTS('',3,(#14476,#14477,#14478,#14479,#14480,
#14481,#14482,#14483,#14484,#14485,#14486,#14487,#14488,#14489,#14490,#14491,
#14492,#14493),.UNSPECIFIED.,.F.,.F.,(4,2,2,2,2,2,2,2,4),(0.,0.079216580773363,
0.158433161546726,0.23764869707457,0.316864232602414,0.396079768130259,
0.475295303658103,0.554511884431466,0.633728465204829),.UNSPECIFIED.);
#389=B_SPLINE_CURVE_WITH_KNOTS('',3,(#14494,#14495,#14496,#14497,#14498,
#14499,#14500,#14501,#14502,#14503,#14504,#14505,#14506,#14507,#14508,#14509,
#14510,#14511),.UNSPECIFIED.,.F.,.F.,(4,2,2,2,2,2,2,2,4),(0.633728465204829,
0.712945045978192,0.792161626751555,0.871377162279399,0.950592697807243,
1.02980823333509,1.10902376886293,1.18824034963629,1.26745693040966),
 .UNSPECIFIED.);
#390=B_SPLINE_CURVE_WITH_KNOTS('',3,(#14514,#14515,#14516,#14517,#14518,
#14519,#14520,#14521,#14522,#14523,#14524,#14525,#14526,#14527),
 .UNSPECIFIED.,.F.,.F.,(4,2,2,2,2,2,4),(0.121154929624516,0.158718019202143,
0.238071711691697,0.317425404181252,0.396779096670807,0.476132789160362,
0.513695878737989),.UNSPECIFIED.);
#497=SHAPE_REPRESENTATION_RELATIONSHIP('SRR','None',#15039,#536);
#536=ADVANCED_BREP_SHAPE_REPRESENTATION('',(#641),#14819);
#590=STYLED_ITEM('',(#15284),#641);
#641=MANIFOLD_SOLID_BREP('Body1',#7709);
#856=FACE_BOUND('',#2173,.T.);
#857=FACE_BOUND('',#2175,.T.);
#858=FACE_BOUND('',#2177,.T.);
#859=FACE_BOUND('',#2179,.T.);
#1081=PLANE('',#9087);
#1082=PLANE('',#9092);
#1083=PLANE('',#9099);
#1084=PLANE('',#9100);
#1512=FACE_OUTER_BOUND('',#2169,.T.);
#1513=FACE_OUTER_BOUND('',#2170,.T.);
#1514=FACE_OUTER_BOUND('',#2171,.T.);
#1515=FACE_OUTER_BOUND('',#2172,.T.);
#1516=FACE_OUTER_BOUND('',#2174,.T.);
#1517=FACE_OUTER_BOUND('',#2176,.T.);
#1518=FACE_OUTER_BOUND('',#2178,.T.);
#2169=EDGE_LOOP('',(#6900,#6901));
#2170=EDGE_LOOP('',(#6902,#6903,#6904,#6905,#6906,#6907,#6908,#6909,#6910));
#2171=EDGE_LOOP('',(#6911,#6912,#6913));
#2172=EDGE_LOOP('',(#6914,#6915,#6916,#6917));
#2173=EDGE_LOOP('',(#6918,#6919,#6920,#6921));
#2174=EDGE_LOOP('',(#6922,#6923,#6924,#6925));
#2175=EDGE_LOOP('',(#6926,#6927));
#2176=EDGE_LOOP('',(#6928));
#2177=EDGE_LOOP('',(#6929));
#2178=EDGE_LOOP('',(#6930));
#2179=EDGE_LOOP('',(#6931));
#2627=LINE('',#14453,#3071);
#2628=LINE('',#14474,#3072);
#2629=LINE('',#14529,#3073);
#2630=LINE('',#14534,#3074);
#2631=LINE('',#14540,#3075);
#3071=VECTOR('',#11466,1.);
#3072=VECTOR('',#11473,0.21);
#3073=VECTOR('',#11478,1.);
#3074=VECTOR('',#11483,1.005);
#3075=VECTOR('',#11490,1.5);
#3525=CIRCLE('',#9088,0.21);
#3526=CIRCLE('',#9090,0.21);
#3527=CIRCLE('',#9091,0.21);
#3528=CIRCLE('',#9094,1.005);
#3529=CIRCLE('',#9095,1.005);
#3530=CIRCLE('',#9097,1.5);
#3531=CIRCLE('',#9098,1.5);
#4152=VERTEX_POINT('',#14451);
#4153=VERTEX_POINT('',#14452);
#4154=VERTEX_POINT('',#14456);
#4155=VERTEX_POINT('',#14471);
#4156=VERTEX_POINT('',#14473);
#4157=VERTEX_POINT('',#14475);
#4158=VERTEX_POINT('',#14512);
#4159=VERTEX_POINT('',#14531);
#4160=VERTEX_POINT('',#14533);
#4161=VERTEX_POINT('',#14537);
#4162=VERTEX_POINT('',#14539);
#5076=EDGE_CURVE('',#4152,#4153,#2627,.T.);
#5077=EDGE_CURVE('',#4152,#4153,#3525,.T.);
#5078=EDGE_CURVE('',#4154,#4152,#387,.T.);
#5079=EDGE_CURVE('',#4155,#4154,#3526,.T.);
#5080=EDGE_CURVE('',#4155,#4156,#2628,.T.);
#5081=EDGE_CURVE('',#4157,#4156,#388,.T.);
#5082=EDGE_CURVE('',#4156,#4157,#389,.T.);
#5083=EDGE_CURVE('',#4158,#4155,#3527,.T.);
#5084=EDGE_CURVE('',#4153,#4158,#390,.T.);
#5085=EDGE_CURVE('',#4158,#4154,#2629,.T.);
#5086=EDGE_CURVE('',#4159,#4159,#3528,.T.);
#5087=EDGE_CURVE('',#4159,#4160,#2630,.T.);
#5088=EDGE_CURVE('',#4160,#4160,#3529,.T.);
#5089=EDGE_CURVE('',#4161,#4161,#3530,.T.);
#5090=EDGE_CURVE('',#4161,#4162,#2631,.T.);
#5091=EDGE_CURVE('',#4162,#4162,#3531,.T.);
#6900=ORIENTED_EDGE('',*,*,#5076,.F.);
#6901=ORIENTED_EDGE('',*,*,#5077,.T.);
#6902=ORIENTED_EDGE('',*,*,#5078,.F.);
#6903=ORIENTED_EDGE('',*,*,#5079,.F.);
#6904=ORIENTED_EDGE('',*,*,#5080,.T.);
#6905=ORIENTED_EDGE('',*,*,#5081,.F.);
#6906=ORIENTED_EDGE('',*,*,#5082,.F.);
#6907=ORIENTED_EDGE('',*,*,#5080,.F.);
#6908=ORIENTED_EDGE('',*,*,#5083,.F.);
#6909=ORIENTED_EDGE('',*,*,#5084,.F.);
#6910=ORIENTED_EDGE('',*,*,#5077,.F.);
#6911=ORIENTED_EDGE('',*,*,#5085,.F.);
#6912=ORIENTED_EDGE('',*,*,#5083,.T.);
#6913=ORIENTED_EDGE('',*,*,#5079,.T.);
#6914=ORIENTED_EDGE('',*,*,#5086,.F.);
#6915=ORIENTED_EDGE('',*,*,#5087,.T.);
#6916=ORIENTED_EDGE('',*,*,#5088,.T.);
#6917=ORIENTED_EDGE('',*,*,#5087,.F.);
#6918=ORIENTED_EDGE('',*,*,#5084,.T.);
#6919=ORIENTED_EDGE('',*,*,#5085,.T.);
#6920=ORIENTED_EDGE('',*,*,#5078,.T.);
#6921=ORIENTED_EDGE('',*,*,#5076,.T.);
#6922=ORIENTED_EDGE('',*,*,#5089,.F.);
#6923=ORIENTED_EDGE('',*,*,#5090,.T.);
#6924=ORIENTED_EDGE('',*,*,#5091,.T.);
#6925=ORIENTED_EDGE('',*,*,#5090,.F.);
#6926=ORIENTED_EDGE('',*,*,#5081,.T.);
#6927=ORIENTED_EDGE('',*,*,#5082,.T.);
#6928=ORIENTED_EDGE('',*,*,#5089,.T.);
#6929=ORIENTED_EDGE('',*,*,#5086,.T.);
#6930=ORIENTED_EDGE('',*,*,#5091,.F.);
#6931=ORIENTED_EDGE('',*,*,#5088,.F.);
#7198=CYLINDRICAL_SURFACE('',#9089,0.21);
#7199=CYLINDRICAL_SURFACE('',#9093,1.005);
#7200=CYLINDRICAL_SURFACE('',#9096,1.5);
#7623=ADVANCED_FACE('',(#1512),#1081,.T.);
#7624=ADVANCED_FACE('',(#1513),#7198,.F.);
#7625=ADVANCED_FACE('',(#1514),#1082,.T.);
#7626=ADVANCED_FACE('',(#1515,#856),#7199,.F.);
#7627=ADVANCED_FACE('',(#1516,#857),#7200,.T.);
#7628=ADVANCED_FACE('',(#1517,#858),#1083,.T.);
#7629=ADVANCED_FACE('',(#1518,#859),#1084,.F.);
#7709=CLOSED_SHELL('',(#7623,#7624,#7625,#7626,#7627,#7628,#7629));
#9086=AXIS2_PLACEMENT_3D('',#14449,#11462,#11463);
#9087=AXIS2_PLACEMENT_3D('',#14450,#11464,#11465);
#9088=AXIS2_PLACEMENT_3D('',#14454,#11467,#11468);
#9089=AXIS2_PLACEMENT_3D('',#14455,#11469,#11470);
#9090=AXIS2_PLACEMENT_3D('',#14472,#11471,#11472);
#9091=AXIS2_PLACEMENT_3D('',#14513,#11474,#11475);
#9092=AXIS2_PLACEMENT_3D('',#14528,#11476,#11477);
#9093=AXIS2_PLACEMENT_3D('',#14530,#11479,#11480);
#9094=AXIS2_PLACEMENT_3D('',#14532,#11481,#11482);
#9095=AXIS2_PLACEMENT_3D('',#14535,#11484,#11485);
#9096=AXIS2_PLACEMENT_3D('',#14536,#11486,#11487);
#9097=AXIS2_PLACEMENT_3D('',#14538,#11488,#11489);
#9098=AXIS2_PLACEMENT_3D('',#14541,#11491,#11492);
#9099=AXIS2_PLACEMENT_3D('',#14542,#11493,#11494);
#9100=AXIS2_PLACEMENT_3D('',#14543,#11495,#11496);
#11462=DIRECTION('axis',(0.,0.,1.));
#11463=DIRECTION('refdir',(1.,0.,0.));
#11464=DIRECTION('center_axis',(0.,0.,1.));
#11465=DIRECTION('ref_axis',(1.,0.,0.));
#11466=DIRECTION('',(0.,1.,0.));
#11467=DIRECTION('center_axis',(0.,0.,1.));
#11468=DIRECTION('ref_axis',(1.,0.,0.));
#11469=DIRECTION('center_axis',(0.,0.,1.));
#11470=DIRECTION('ref_axis',(1.,0.,0.));
#11471=DIRECTION('center_axis',(0.,0.,1.));
#11472=DIRECTION('ref_axis',(1.,0.,0.));
#11473=DIRECTION('',(0.,0.,1.));
#11474=DIRECTION('center_axis',(0.,0.,1.));
#11475=DIRECTION('ref_axis',(1.,0.,0.));
#11476=DIRECTION('center_axis',(0.,0.,1.));
#11477=DIRECTION('ref_axis',(1.,0.,0.));
#11478=DIRECTION('',(0.,-1.,0.));
#11479=DIRECTION('center_axis',(0.,1.,0.));
#11480=DIRECTION('ref_axis',(1.,0.,0.));
#11481=DIRECTION('center_axis',(0.,-1.,0.));
#11482=DIRECTION('ref_axis',(1.,0.,0.));
#11483=DIRECTION('',(0.,-1.,0.));
#11484=DIRECTION('center_axis',(0.,-1.,0.));
#11485=DIRECTION('ref_axis',(1.,0.,0.));
#11486=DIRECTION('center_axis',(0.,1.,0.));
#11487=DIRECTION('ref_axis',(1.,0.,0.));
#11488=DIRECTION('center_axis',(0.,1.,0.));
#11489=DIRECTION('ref_axis',(1.,0.,0.));
#11490=DIRECTION('',(0.,-1.,0.));
#11491=DIRECTION('center_axis',(0.,1.,0.));
#11492=DIRECTION('ref_axis',(1.,0.,0.));
#11493=DIRECTION('center_axis',(0.,1.,0.));
#11494=DIRECTION('ref_axis',(1.,0.,0.));
#11495=DIRECTION('center_axis',(0.,1.,0.));
#11496=DIRECTION('ref_axis',(1.,0.,0.));
#14449=CARTESIAN_POINT('',(0.,0.,0.));
#14450=CARTESIAN_POINT('Origin',(0.,1.1,7.99));
#14451=CARTESIAN_POINT('',(0.172988438920056,0.980941191002085,7.99));
#14452=CARTESIAN_POINT('',(0.172988438920056,1.21905880899792,7.99));
#14453=CARTESIAN_POINT('',(0.172988438920056,0.7,7.99));
#14454=CARTESIAN_POINT('Origin',(0.,1.1,7.99));
#14455=CARTESIAN_POINT('Origin',(0.,1.1,7.99));
#14456=CARTESIAN_POINT('',(-0.172988438920056,0.980941191002085,7.99));
#14457=CARTESIAN_POINT('Ctrl Pts',(-0.172988438920056,0.980941191002085,
7.99));
#14458=CARTESIAN_POINT('Ctrl Pts',(-0.165594865311315,0.970198577604708,
7.99129192197638));
#14459=CARTESIAN_POINT('Ctrl Pts',(-0.157297138725606,0.960312290627256,
7.99265394943905));
#14460=CARTESIAN_POINT('Ctrl Pts',(-0.129892073845076,0.932907225746726,
7.9967480843909));
#14461=CARTESIAN_POINT('Ctrl Pts',(-0.106330167759285,0.916757943667051,
7.99969589327638));
#14462=CARTESIAN_POINT('Ctrl Pts',(-0.0546129046324106,0.895302206035095,
8.00385029472357));
#14463=CARTESIAN_POINT('Ctrl Pts',(-0.0264512308298516,0.89,8.005));
#14464=CARTESIAN_POINT('Ctrl Pts',(0.0264512308298515,0.89,8.005));
#14465=CARTESIAN_POINT('Ctrl Pts',(0.0546129046324105,0.895302206035094,
8.00385029472357));
#14466=CARTESIAN_POINT('Ctrl Pts',(0.106330167759284,0.916757943667051,
7.99969589327638));
#14467=CARTESIAN_POINT('Ctrl Pts',(0.129892073845076,0.932907225746726,
7.9967480843909));
#14468=CARTESIAN_POINT('Ctrl Pts',(0.157297138725606,0.960312290627256,
7.99265394943905));
#14469=CARTESIAN_POINT('Ctrl Pts',(0.165594865311314,0.970198577604708,
7.99129192197638));
#14470=CARTESIAN_POINT('Ctrl Pts',(0.172988438920056,0.980941191002085,
7.99));
#14471=CARTESIAN_POINT('',(-0.21,1.1,7.99));
#14472=CARTESIAN_POINT('Origin',(0.,1.1,7.99));
#14473=CARTESIAN_POINT('',(-0.21,1.1,8.48522725533839));
#14474=CARTESIAN_POINT('',(-0.21,1.1,7.99));
#14475=CARTESIAN_POINT('',(0.21,1.1,8.48522725533839));
#14476=CARTESIAN_POINT('Ctrl Pts',(0.21,1.1,8.48522725533839));
#14477=CARTESIAN_POINT('Ctrl Pts',(0.21,1.07359447307555,8.48522725533839));
#14478=CARTESIAN_POINT('Ctrl Pts',(0.204715737269596,1.04545292590929,8.48600415954412));
#14479=CARTESIAN_POINT('Ctrl Pts',(0.183273763036331,0.993723731094873,
8.48880073282317));
#14480=CARTESIAN_POINT('Ctrl Pts',(0.167117923970394,0.970133075872044,
8.49077897157582));
#14481=CARTESIAN_POINT('Ctrl Pts',(0.129867169887369,0.932882321789019,
8.49448481141327));
#14482=CARTESIAN_POINT('Ctrl Pts',(0.106276408305765,0.916726289998648,
8.49645455657129));
#14483=CARTESIAN_POINT('Ctrl Pts',(0.0545468514059001,0.895284175173782,
8.49923165515646));
#14484=CARTESIAN_POINT('Ctrl Pts',(0.0264051785092814,0.89,8.5));
#14485=CARTESIAN_POINT('Ctrl Pts',(-0.0264051785092814,0.89,8.5));
#14486=CARTESIAN_POINT('Ctrl Pts',(-0.0545468514059001,0.895284175173782,
8.49923165515646));
#14487=CARTESIAN_POINT('Ctrl Pts',(-0.106276408305765,0.916726289998648,
8.49645455657129));
#14488=CARTESIAN_POINT('Ctrl Pts',(-0.129867169887369,0.932882321789019,
8.49448481141327));
#14489=CARTESIAN_POINT('Ctrl Pts',(-0.167117923970394,0.970133075872044,
8.49077897157582));
#14490=CARTESIAN_POINT('Ctrl Pts',(-0.183273763036331,0.993723731094873,
8.48880073282317));
#14491=CARTESIAN_POINT('Ctrl Pts',(-0.204715737269596,1.04545292590929,
8.48600415954412));
#14492=CARTESIAN_POINT('Ctrl Pts',(-0.21,1.07359447307555,8.48522725533839));
#14493=CARTESIAN_POINT('Ctrl Pts',(-0.21,1.1,8.48522725533839));
#14494=CARTESIAN_POINT('Ctrl Pts',(-0.21,1.1,8.48522725533839));
#14495=CARTESIAN_POINT('Ctrl Pts',(-0.21,1.12640552692445,8.48522725533839));
#14496=CARTESIAN_POINT('Ctrl Pts',(-0.204715737269596,1.15454707409071,
8.48600415954412));
#14497=CARTESIAN_POINT('Ctrl Pts',(-0.183273763036331,1.20627626890513,
8.48880073282317));
#14498=CARTESIAN_POINT('Ctrl Pts',(-0.167117923970394,1.22986692412796,
8.49077897157582));
#14499=CARTESIAN_POINT('Ctrl Pts',(-0.129867169887369,1.26711767821098,
8.49448481141327));
#14500=CARTESIAN_POINT('Ctrl Pts',(-0.106276408305765,1.28327371000135,
8.49645455657129));
#14501=CARTESIAN_POINT('Ctrl Pts',(-0.0545468514059002,1.30471582482622,
8.49923165515646));
#14502=CARTESIAN_POINT('Ctrl Pts',(-0.0264051785092814,1.31,8.5));
#14503=CARTESIAN_POINT('Ctrl Pts',(0.0264051785092814,1.31,8.5));
#14504=CARTESIAN_POINT('Ctrl Pts',(0.0545468514059003,1.30471582482622,
8.49923165515645));
#14505=CARTESIAN_POINT('Ctrl Pts',(0.106276408305765,1.28327371000135,8.49645455657129));
#14506=CARTESIAN_POINT('Ctrl Pts',(0.129867169887369,1.26711767821098,8.49448481141327));
#14507=CARTESIAN_POINT('Ctrl Pts',(0.167117923970394,1.22986692412796,8.49077897157582));
#14508=CARTESIAN_POINT('Ctrl Pts',(0.183273763036332,1.20627626890513,8.48880073282317));
#14509=CARTESIAN_POINT('Ctrl Pts',(0.204715737269596,1.15454707409071,8.48600415954412));
#14510=CARTESIAN_POINT('Ctrl Pts',(0.21,1.12640552692445,8.48522725533839));
#14511=CARTESIAN_POINT('Ctrl Pts',(0.21,1.1,8.48522725533839));
#14512=CARTESIAN_POINT('',(-0.172988438920056,1.21905880899792,7.99));
#14513=CARTESIAN_POINT('Origin',(0.,1.1,7.99));
#14514=CARTESIAN_POINT('Ctrl Pts',(0.172988438920056,1.21905880899792,7.99));
#14515=CARTESIAN_POINT('Ctrl Pts',(0.165594865311314,1.22980142239529,7.99129192197638));
#14516=CARTESIAN_POINT('Ctrl Pts',(0.157297138725606,1.23968770937274,7.99265394943905));
#14517=CARTESIAN_POINT('Ctrl Pts',(0.129892073845076,1.26709277425327,7.9967480843909));
#14518=CARTESIAN_POINT('Ctrl Pts',(0.106330167759284,1.28324205633295,7.99969589327638));
#14519=CARTESIAN_POINT('Ctrl Pts',(0.0546129046324105,1.30469779396491,
8.00385029472357));
#14520=CARTESIAN_POINT('Ctrl Pts',(0.0264512308298516,1.31,8.005));
#14521=CARTESIAN_POINT('Ctrl Pts',(-0.0264512308298516,1.31,8.005));
#14522=CARTESIAN_POINT('Ctrl Pts',(-0.0546129046324105,1.30469779396491,
8.00385029472357));
#14523=CARTESIAN_POINT('Ctrl Pts',(-0.106330167759284,1.28324205633295,
7.99969589327638));
#14524=CARTESIAN_POINT('Ctrl Pts',(-0.129892073845076,1.26709277425327,
7.9967480843909));
#14525=CARTESIAN_POINT('Ctrl Pts',(-0.157297138725606,1.23968770937274,
7.99265394943905));
#14526=CARTESIAN_POINT('Ctrl Pts',(-0.165594865311314,1.22980142239529,
7.99129192197638));
#14527=CARTESIAN_POINT('Ctrl Pts',(-0.172988438920056,1.21905880899792,
7.99));
#14528=CARTESIAN_POINT('Origin',(0.,1.1,7.99));
#14529=CARTESIAN_POINT('',(-0.172988438920056,0.7,7.99));
#14530=CARTESIAN_POINT('Origin',(0.,0.7,7.));
#14531=CARTESIAN_POINT('',(-1.005,1.5,7.));
#14532=CARTESIAN_POINT('Origin',(0.,1.5,7.));
#14533=CARTESIAN_POINT('',(-1.005,0.7,7.));
#14534=CARTESIAN_POINT('',(-1.005,0.7,7.));
#14535=CARTESIAN_POINT('Origin',(0.,0.7,7.));
#14536=CARTESIAN_POINT('Origin',(0.,0.7,7.));
#14537=CARTESIAN_POINT('',(-1.5,1.5,7.));
#14538=CARTESIAN_POINT('Origin',(0.,1.5,7.));
#14539=CARTESIAN_POINT('',(-1.5,0.7,7.));
#14540=CARTESIAN_POINT('',(-1.5,0.7,7.));
#14541=CARTESIAN_POINT('Origin',(0.,0.7,7.));
#14542=CARTESIAN_POINT('Origin',(0.,1.5,7.));
#14543=CARTESIAN_POINT('Origin',(0.,0.7,7.));
#14774=UNCERTAINTY_MEASURE_WITH_UNIT(LENGTH_MEASURE(0.001),#14823,
'DISTANCE_ACCURACY_VALUE',
'Maximum model space distance between geometric entities at asserted c
onnectivities');
#14777=UNCERTAINTY_MEASURE_WITH_UNIT(LENGTH_MEASURE(0.001),#14823,
'DISTANCE_ACCURACY_VALUE',
'Maximum model space distance between geometric entities at asserted c
onnectivities');
#14819=(
GEOMETRIC_REPRESENTATION_CONTEXT(3)
GLOBAL_UNCERTAINTY_ASSIGNED_CONTEXT((#14774))
GLOBAL_UNIT_ASSIGNED_CONTEXT((#14823,#14825,#14826))
REPRESENTATION_CONTEXT('','3D')
);
#14822=(
GEOMETRIC_REPRESENTATION_CONTEXT(3)
GLOBAL_UNCERTAINTY_ASSIGNED_CONTEXT((#14777))
GLOBAL_UNIT_ASSIGNED_CONTEXT((#14823,#14825,#14826))
REPRESENTATION_CONTEXT('','3D')
);
#14823=(
LENGTH_UNIT()
NAMED_UNIT(*)
SI_UNIT(.CENTI.,.METRE.)
);
#14825=(
NAMED_UNIT(*)
PLANE_ANGLE_UNIT()
SI_UNIT($,.RADIAN.)
);
#14826=(
NAMED_UNIT(*)
SI_UNIT($,.STERADIAN.)
SOLID_ANGLE_UNIT()
);
#14868=SHAPE_DEFINITION_REPRESENTATION(#14978,#15039);
#14978=PRODUCT_DEFINITION_SHAPE('',$,#15084);
#15039=SHAPE_REPRESENTATION('',(#9086),#14819);
#15042=PRODUCT_DEFINITION_CONTEXT('part definition',#15176,'design');
#15084=PRODUCT_DEFINITION('Test bearing collar (1)',
'Test bearing collar (1)',#15128,#15042);
#15128=PRODUCT_DEFINITION_FORMATION('',$,#15219);
#15176=APPLICATION_CONTEXT(
'Core Data for Automotive Mechanical Design Process');
#15177=PRODUCT_CONTEXT('part definition',#15176,'mechanical');
#15219=PRODUCT('Test bearing collar (1)','Test bearing collar (1)',
'Test bearing collar (1)',(#15177));
#15278=COLOUR_RGB('Grey',0.48,0.52,0.57);
#15279=FILL_AREA_STYLE_COLOUR('',#15278);
#15280=FILL_AREA_STYLE('',(#15279));
#15281=SURFACE_STYLE_FILL_AREA(#15280);
#15282=SURFACE_SIDE_STYLE('',(#15281));
#15283=SURFACE_STYLE_USAGE(.BOTH.,#15282);
#15284=PRESENTATION_STYLE_ASSIGNMENT((#15283));
ENDSEC;
END-ISO-10303-21;
